ISO-10303-21;
HEADER;
/* Generated by software containing ST-Developer
 * from STEP Tools, Inc. (www.steptools.com) 
 */

FILE_DESCRIPTION(
/* description */ (''),
/* implementation_level */ '2;1');

FILE_NAME(
/* name */ '08_Thrust_Ball_Bearing_51104_20x35x10.step',
/* time_stamp */ '2026-10-26T03:50:32-07:00',
/* author */ (''),
/* organization */ (''),
/* preprocessor_version */ 'ST-DEVELOPER v20.2',
/* originating_system */ 'Autodesk Translation Framework v15.15.0.0',
/* authorisation */ '');

FILE_SCHEMA (('AUTOMOTIVE_DESIGN { 1 0 10303 214 3 1 1 }'));
ENDSEC;

DATA;
#10=MECHANICAL_DESIGN_GEOMETRIC_PRESENTATION_REPRESENTATION('',(#1055),#76660);
#1015=SHAPE_REPRESENTATION_RELATIONSHIP('SRR','None',#76752,#1035);
#1035=ADVANCED_BREP_SHAPE_REPRESENTATION('',(#1075),#76656);
#1055=STYLED_ITEM('',(#76906),#1075);
#1075=MANIFOLD_SOLID_BREP('Bearing 51104',#26680);
#1407=CYLINDRICAL_SURFACE('',#28531,1.56);
#1408=CYLINDRICAL_SURFACE('',#28533,1.05);
#1409=CYLINDRICAL_SURFACE('',#28540,1.75);
#1410=CYLINDRICAL_SURFACE('',#28543,1.56);
#1411=CYLINDRICAL_SURFACE('',#28547,1.72);
#1412=CYLINDRICAL_SURFACE('',#28553,1.);
#1413=CYLINDRICAL_SURFACE('',#28557,1.24);
#1644=FACE_BOUND('',#5217,.T.);
#1645=FACE_BOUND('',#5221,.T.);
#1646=FACE_BOUND('',#5224,.T.);
#1647=FACE_BOUND('',#5228,.T.);
#1648=FACE_BOUND('',#5231,.T.);
#1649=FACE_BOUND('',#5234,.T.);
#2185=PLANE('',#28536);
#2186=PLANE('',#28542);
#2187=PLANE('',#28545);
#2188=PLANE('',#28551);
#2189=PLANE('',#28555);
#2190=PLANE('',#28559);
#3569=FACE_OUTER_BOUND('',#5212,.T.);
#3570=FACE_OUTER_BOUND('',#5213,.T.);
#3571=FACE_OUTER_BOUND('',#5214,.T.);
#3572=FACE_OUTER_BOUND('',#5215,.T.);
#3573=FACE_OUTER_BOUND('',#5216,.T.);
#3574=FACE_OUTER_BOUND('',#5218,.T.);
#3575=FACE_OUTER_BOUND('',#5219,.T.);
#3576=FACE_OUTER_BOUND('',#5220,.T.);
#3577=FACE_OUTER_BOUND('',#5222,.T.);
#3578=FACE_OUTER_BOUND('',#5223,.T.);
#3579=FACE_OUTER_BOUND('',#5225,.T.);
#3580=FACE_OUTER_BOUND('',#5226,.T.);
#3581=FACE_OUTER_BOUND('',#5227,.T.);
#3582=FACE_OUTER_BOUND('',#5229,.T.);
#3583=FACE_OUTER_BOUND('',#5230,.T.);
#3584=FACE_OUTER_BOUND('',#5232,.T.);
#3585=FACE_OUTER_BOUND('',#5233,.T.);
#5212=EDGE_LOOP('',(#22359,#22360,#22361,#22362));
#5213=EDGE_LOOP('',(#22363,#22364,#22365,#22366));
#5214=EDGE_LOOP('',(#22367,#22368,#22369,#22370));
#5215=EDGE_LOOP('',(#22371,#22372,#22373,#22374));
#5216=EDGE_LOOP('',(#22375));
#5217=EDGE_LOOP('',(#22376));
#5218=EDGE_LOOP('',(#22377,#22378,#22379,#22380));
#5219=EDGE_LOOP('',(#22381,#22382,#22383,#22384));
#5220=EDGE_LOOP('',(#22385));
#5221=EDGE_LOOP('',(#22386));
#5222=EDGE_LOOP('',(#22387,#22388,#22389,#22390));
#5223=EDGE_LOOP('',(#22391));
#5224=EDGE_LOOP('',(#22392));
#5225=EDGE_LOOP('',(#22393,#22394,#22395,#22396));
#5226=EDGE_LOOP('',(#22397,#22398,#22399,#22400));
#5227=EDGE_LOOP('',(#22401));
#5228=EDGE_LOOP('',(#22402));
#5229=EDGE_LOOP('',(#22403,#22404,#22405,#22406));
#5230=EDGE_LOOP('',(#22407));
#5231=EDGE_LOOP('',(#22408));
#5232=EDGE_LOOP('',(#22409,#22410,#22411,#22412));
#5233=EDGE_LOOP('',(#22413));
#5234=EDGE_LOOP('',(#22414));
#6305=CIRCLE('',#28527,1.49);
#6306=CIRCLE('',#28528,1.56);
#6307=CIRCLE('',#28530,1.56);
#6308=CIRCLE('',#28532,1.56);
#6309=CIRCLE('',#28534,1.05);
#6310=CIRCLE('',#28535,1.05);
#6311=CIRCLE('',#28537,1.7);
#6312=CIRCLE('',#28539,1.75);
#6313=CIRCLE('',#28541,1.75);
#6314=CIRCLE('',#28544,1.56);
#6315=CIRCLE('',#28546,1.72);
#6316=CIRCLE('',#28548,1.72);
#6317=CIRCLE('',#28550,1.67);
#6318=CIRCLE('',#28552,1.);
#6319=CIRCLE('',#28554,1.);
#6320=CIRCLE('',#28556,1.24);
#6321=CIRCLE('',#28558,1.24);
#8042=LINE('',#63484,#10198);
#8043=LINE('',#63489,#10199);
#8044=LINE('',#63492,#10200);
#8045=LINE('',#63498,#10201);
#8046=LINE('',#63506,#10202);
#8047=LINE('',#63510,#10203);
#8048=LINE('',#63515,#10204);
#8049=LINE('',#63522,#10205);
#8050=LINE('',#63526,#10206);
#8051=LINE('',#63532,#10207);
#8052=LINE('',#63539,#10208);
#10198=VECTOR('',#34041,1.53);
#10199=VECTOR('',#34048,1.53);
#10200=VECTOR('',#34051,1.56);
#10201=VECTOR('',#34058,1.05);
#10202=VECTOR('',#34069,1.725);
#10203=VECTOR('',#34074,1.75);
#10204=VECTOR('',#34081,1.56);
#10205=VECTOR('',#34090,1.72);
#10206=VECTOR('',#34095,1.695);
#10207=VECTOR('',#34102,1.);
#10208=VECTOR('',#34111,1.24);
#12521=VERTEX_POINT('',#63481);
#12522=VERTEX_POINT('',#63483);
#12523=VERTEX_POINT('',#63487);
#12524=VERTEX_POINT('',#63491);
#12525=VERTEX_POINT('',#63495);
#12526=VERTEX_POINT('',#63497);
#12527=VERTEX_POINT('',#63501);
#12528=VERTEX_POINT('',#63504);
#12529=VERTEX_POINT('',#63508);
#12530=VERTEX_POINT('',#63513);
#12531=VERTEX_POINT('',#63517);
#12532=VERTEX_POINT('',#63520);
#12533=VERTEX_POINT('',#63524);
#12534=VERTEX_POINT('',#63528);
#12535=VERTEX_POINT('',#63531);
#12536=VERTEX_POINT('',#63535);
#12537=VERTEX_POINT('',#63538);
#15902=EDGE_CURVE('',#12521,#12521,#6305,.T.);
#15903=EDGE_CURVE('',#12521,#12522,#8042,.T.);
#15904=EDGE_CURVE('',#12522,#12522,#6306,.T.);
#15905=EDGE_CURVE('',#12523,#12523,#6307,.T.);
#15906=EDGE_CURVE('',#12523,#12521,#8043,.T.);
#15907=EDGE_CURVE('',#12523,#12524,#8044,.T.);
#15908=EDGE_CURVE('',#12524,#12524,#6308,.T.);
#15909=EDGE_CURVE('',#12525,#12525,#6309,.T.);
#15910=EDGE_CURVE('',#12525,#12526,#8045,.T.);
#15911=EDGE_CURVE('',#12526,#12526,#6310,.T.);
#15912=EDGE_CURVE('',#12527,#12527,#6311,.T.);
#15913=EDGE_CURVE('',#12528,#12528,#6312,.T.);
#15914=EDGE_CURVE('',#12528,#12527,#8046,.T.);
#15915=EDGE_CURVE('',#12529,#12529,#6313,.T.);
#15916=EDGE_CURVE('',#12529,#12528,#8047,.T.);
#15917=EDGE_CURVE('',#12530,#12530,#6314,.T.);
#15918=EDGE_CURVE('',#12530,#12522,#8048,.T.);
#15919=EDGE_CURVE('',#12531,#12531,#6315,.T.);
#15920=EDGE_CURVE('',#12532,#12532,#6316,.T.);
#15921=EDGE_CURVE('',#12532,#12531,#8049,.T.);
#15922=EDGE_CURVE('',#12533,#12533,#6317,.T.);
#15923=EDGE_CURVE('',#12533,#12532,#8050,.T.);
#15924=EDGE_CURVE('',#12534,#12534,#6318,.T.);
#15925=EDGE_CURVE('',#12534,#12535,#8051,.T.);
#15926=EDGE_CURVE('',#12535,#12535,#6319,.T.);
#15927=EDGE_CURVE('',#12536,#12536,#6320,.T.);
#15928=EDGE_CURVE('',#12536,#12537,#8052,.T.);
#15929=EDGE_CURVE('',#12537,#12537,#6321,.T.);
#22359=ORIENTED_EDGE('',*,*,#15902,.T.);
#22360=ORIENTED_EDGE('',*,*,#15903,.T.);
#22361=ORIENTED_EDGE('',*,*,#15904,.F.);
#22362=ORIENTED_EDGE('',*,*,#15903,.F.);
#22363=ORIENTED_EDGE('',*,*,#15905,.F.);
#22364=ORIENTED_EDGE('',*,*,#15906,.T.);
#22365=ORIENTED_EDGE('',*,*,#15902,.F.);
#22366=ORIENTED_EDGE('',*,*,#15906,.F.);
#22367=ORIENTED_EDGE('',*,*,#15905,.T.);
#22368=ORIENTED_EDGE('',*,*,#15907,.T.);
#22369=ORIENTED_EDGE('',*,*,#15908,.T.);
#22370=ORIENTED_EDGE('',*,*,#15907,.F.);
#22371=ORIENTED_EDGE('',*,*,#15909,.T.);
#22372=ORIENTED_EDGE('',*,*,#15910,.T.);
#22373=ORIENTED_EDGE('',*,*,#15911,.F.);
#22374=ORIENTED_EDGE('',*,*,#15910,.F.);
#22375=ORIENTED_EDGE('',*,*,#15912,.F.);
#22376=ORIENTED_EDGE('',*,*,#15911,.T.);
#22377=ORIENTED_EDGE('',*,*,#15913,.F.);
#22378=ORIENTED_EDGE('',*,*,#15914,.T.);
#22379=ORIENTED_EDGE('',*,*,#15912,.T.);
#22380=ORIENTED_EDGE('',*,*,#15914,.F.);
#22381=ORIENTED_EDGE('',*,*,#15915,.F.);
#22382=ORIENTED_EDGE('',*,*,#15916,.T.);
#22383=ORIENTED_EDGE('',*,*,#15913,.T.);
#22384=ORIENTED_EDGE('',*,*,#15916,.F.);
#22385=ORIENTED_EDGE('',*,*,#15915,.T.);
#22386=ORIENTED_EDGE('',*,*,#15908,.F.);
#22387=ORIENTED_EDGE('',*,*,#15917,.F.);
#22388=ORIENTED_EDGE('',*,*,#15918,.T.);
#22389=ORIENTED_EDGE('',*,*,#15904,.T.);
#22390=ORIENTED_EDGE('',*,*,#15918,.F.);
#22391=ORIENTED_EDGE('',*,*,#15919,.F.);
#22392=ORIENTED_EDGE('',*,*,#15917,.T.);
#22393=ORIENTED_EDGE('',*,*,#15920,.F.);
#22394=ORIENTED_EDGE('',*,*,#15921,.T.);
#22395=ORIENTED_EDGE('',*,*,#15919,.T.);
#22396=ORIENTED_EDGE('',*,*,#15921,.F.);
#22397=ORIENTED_EDGE('',*,*,#15922,.F.);
#22398=ORIENTED_EDGE('',*,*,#15923,.T.);
#22399=ORIENTED_EDGE('',*,*,#15920,.T.);
#22400=ORIENTED_EDGE('',*,*,#15923,.F.);
#22401=ORIENTED_EDGE('',*,*,#15922,.T.);
#22402=ORIENTED_EDGE('',*,*,#15924,.F.);
#22403=ORIENTED_EDGE('',*,*,#15924,.T.);
#22404=ORIENTED_EDGE('',*,*,#15925,.T.);
#22405=ORIENTED_EDGE('',*,*,#15926,.F.);
#22406=ORIENTED_EDGE('',*,*,#15925,.F.);
#22407=ORIENTED_EDGE('',*,*,#15927,.F.);
#22408=ORIENTED_EDGE('',*,*,#15926,.T.);
#22409=ORIENTED_EDGE('',*,*,#15927,.T.);
#22410=ORIENTED_EDGE('',*,*,#15928,.T.);
#22411=ORIENTED_EDGE('',*,*,#15929,.F.);
#22412=ORIENTED_EDGE('',*,*,#15928,.F.);
#22413=ORIENTED_EDGE('',*,*,#15929,.T.);
#22414=ORIENTED_EDGE('',*,*,#15909,.F.);
#25098=CONICAL_SURFACE('',#28526,1.53,0.785398163397458);
#25099=CONICAL_SURFACE('',#28529,1.53,0.785398163397447);
#25100=CONICAL_SURFACE('',#28538,1.725,0.785398163397451);
#25101=CONICAL_SURFACE('',#28549,1.695,0.785398163397442);
#26157=ADVANCED_FACE('',(#3569),#25098,.T.);
#26158=ADVANCED_FACE('',(#3570),#25099,.T.);
#26159=ADVANCED_FACE('',(#3571),#1407,.T.);
#26160=ADVANCED_FACE('',(#3572),#1408,.F.);
#26161=ADVANCED_FACE('',(#3573,#1644),#2185,.T.);
#26162=ADVANCED_FACE('',(#3574),#25100,.T.);
#26163=ADVANCED_FACE('',(#3575),#1409,.T.);
#26164=ADVANCED_FACE('',(#3576,#1645),#2186,.T.);
#26165=ADVANCED_FACE('',(#3577),#1410,.T.);
#26166=ADVANCED_FACE('',(#3578,#1646),#2187,.T.);
#26167=ADVANCED_FACE('',(#3579),#1411,.T.);
#26168=ADVANCED_FACE('',(#3580),#25101,.T.);
#26169=ADVANCED_FACE('',(#3581,#1647),#2188,.T.);
#26170=ADVANCED_FACE('',(#3582),#1412,.F.);
#26171=ADVANCED_FACE('',(#3583,#1648),#2189,.T.);
#26172=ADVANCED_FACE('',(#3584),#1413,.F.);
#26173=ADVANCED_FACE('',(#3585,#1649),#2190,.T.);
#26680=CLOSED_SHELL('',(#26157,#26158,#26159,#26160,#26161,#26162,#26163,
#26164,#26165,#26166,#26167,#26168,#26169,#26170,#26171,#26172,#26173));
#28525=AXIS2_PLACEMENT_3D('',#63479,#34035,#34036);
#28526=AXIS2_PLACEMENT_3D('',#63480,#34037,#34038);
#28527=AXIS2_PLACEMENT_3D('',#63482,#34039,#34040);
#28528=AXIS2_PLACEMENT_3D('',#63485,#34042,#34043);
#28529=AXIS2_PLACEMENT_3D('',#63486,#34044,#34045);
#28530=AXIS2_PLACEMENT_3D('',#63488,#34046,#34047);
#28531=AXIS2_PLACEMENT_3D('',#63490,#34049,#34050);
#28532=AXIS2_PLACEMENT_3D('',#63493,#34052,#34053);
#28533=AXIS2_PLACEMENT_3D('',#63494,#34054,#34055);
#28534=AXIS2_PLACEMENT_3D('',#63496,#34056,#34057);
#28535=AXIS2_PLACEMENT_3D('',#63499,#34059,#34060);
#28536=AXIS2_PLACEMENT_3D('',#63500,#34061,#34062);
#28537=AXIS2_PLACEMENT_3D('',#63502,#34063,#34064);
#28538=AXIS2_PLACEMENT_3D('',#63503,#34065,#34066);
#28539=AXIS2_PLACEMENT_3D('',#63505,#34067,#34068);
#28540=AXIS2_PLACEMENT_3D('',#63507,#34070,#34071);
#28541=AXIS2_PLACEMENT_3D('',#63509,#34072,#34073);
#28542=AXIS2_PLACEMENT_3D('',#63511,#34075,#34076);
#28543=AXIS2_PLACEMENT_3D('',#63512,#34077,#34078);
#28544=AXIS2_PLACEMENT_3D('',#63514,#34079,#34080);
#28545=AXIS2_PLACEMENT_3D('',#63516,#34082,#34083);
#28546=AXIS2_PLACEMENT_3D('',#63518,#34084,#34085);
#28547=AXIS2_PLACEMENT_3D('',#63519,#34086,#34087);
#28548=AXIS2_PLACEMENT_3D('',#63521,#34088,#34089);
#28549=AXIS2_PLACEMENT_3D('',#63523,#34091,#34092);
#28550=AXIS2_PLACEMENT_3D('',#63525,#34093,#34094);
#28551=AXIS2_PLACEMENT_3D('',#63527,#34096,#34097);
#28552=AXIS2_PLACEMENT_3D('',#63529,#34098,#34099);
#28553=AXIS2_PLACEMENT_3D('',#63530,#34100,#34101);
#28554=AXIS2_PLACEMENT_3D('',#63533,#34103,#34104);
#28555=AXIS2_PLACEMENT_3D('',#63534,#34105,#34106);
#28556=AXIS2_PLACEMENT_3D('',#63536,#34107,#34108);
#28557=AXIS2_PLACEMENT_3D('',#63537,#34109,#34110);
#28558=AXIS2_PLACEMENT_3D('',#63540,#34112,#34113);
#28559=AXIS2_PLACEMENT_3D('',#63541,#34114,#34115);
#34035=DIRECTION('axis',(0.,0.,1.));
#34036=DIRECTION('refdir',(1.,0.,0.));
#34037=DIRECTION('center_axis',(1.,0.,0.));
#34038=DIRECTION('ref_axis',(0.,1.,0.));
#34039=DIRECTION('center_axis',(1.,0.,0.));
#34040=DIRECTION('ref_axis',(0.,0.,-1.));
#34041=DIRECTION('',(0.707106781186541,-0.707106781186554,-8.65956056235502E-17));
#34042=DIRECTION('center_axis',(1.,0.,0.));
#34043=DIRECTION('ref_axis',(0.,1.,0.));
#34044=DIRECTION('center_axis',(-1.,0.,0.));
#34045=DIRECTION('ref_axis',(0.,1.,0.));
#34046=DIRECTION('center_axis',(-1.,0.,0.));
#34047=DIRECTION('ref_axis',(0.,1.,0.));
#34048=DIRECTION('',(0.707106781186548,0.707106781186547,8.65956056235492E-17));
#34049=DIRECTION('center_axis',(1.,0.,0.));
#34050=DIRECTION('ref_axis',(0.,1.,0.));
#34051=DIRECTION('',(-1.,0.,0.));
#34052=DIRECTION('center_axis',(1.,0.,0.));
#34053=DIRECTION('ref_axis',(0.,0.,-1.));
#34054=DIRECTION('center_axis',(1.,0.,0.));
#34055=DIRECTION('ref_axis',(0.,1.,0.));
#34056=DIRECTION('center_axis',(1.,0.,0.));
#34057=DIRECTION('ref_axis',(0.,0.,-1.));
#34058=DIRECTION('',(-1.,0.,0.));
#34059=DIRECTION('center_axis',(1.,0.,0.));
#34060=DIRECTION('ref_axis',(0.,0.,-1.));
#34061=DIRECTION('center_axis',(-1.,0.,0.));
#34062=DIRECTION('ref_axis',(0.,0.,1.));
#34063=DIRECTION('center_axis',(1.,0.,0.));
#34064=DIRECTION('ref_axis',(0.,0.,-1.));
#34065=DIRECTION('center_axis',(1.,0.,0.));
#34066=DIRECTION('ref_axis',(0.,1.,0.));
#34067=DIRECTION('center_axis',(1.,0.,0.));
#34068=DIRECTION('ref_axis',(0.,0.,-1.));
#34069=DIRECTION('',(-0.707106781186546,0.707106781186549,8.65956056235495E-17));
#34070=DIRECTION('center_axis',(1.,0.,0.));
#34071=DIRECTION('ref_axis',(0.,1.,0.));
#34072=DIRECTION('center_axis',(1.,0.,0.));
#34073=DIRECTION('ref_axis',(0.,0.,-1.));
#34074=DIRECTION('',(-1.,0.,0.));
#34075=DIRECTION('center_axis',(1.,0.,0.));
#34076=DIRECTION('ref_axis',(0.,0.,-1.));
#34077=DIRECTION('center_axis',(1.,0.,0.));
#34078=DIRECTION('ref_axis',(0.,1.,0.));
#34079=DIRECTION('center_axis',(1.,0.,0.));
#34080=DIRECTION('ref_axis',(0.,0.,-1.));
#34081=DIRECTION('',(-1.,0.,0.));
#34082=DIRECTION('center_axis',(-1.,0.,0.));
#34083=DIRECTION('ref_axis',(0.,0.,1.));
#34084=DIRECTION('center_axis',(1.,0.,0.));
#34085=DIRECTION('ref_axis',(0.,0.,-1.));
#34086=DIRECTION('center_axis',(1.,0.,0.));
#34087=DIRECTION('ref_axis',(0.,1.,0.));
#34088=DIRECTION('center_axis',(1.,0.,0.));
#34089=DIRECTION('ref_axis',(0.,0.,-1.));
#34090=DIRECTION('',(-1.,0.,0.));
#34091=DIRECTION('center_axis',(-1.,0.,0.));
#34092=DIRECTION('ref_axis',(0.,1.,0.));
#34093=DIRECTION('center_axis',(1.,0.,0.));
#34094=DIRECTION('ref_axis',(0.,0.,-1.));
#34095=DIRECTION('',(-0.707106781186552,-0.707106781186543,-8.65956056235488E-17));
#34096=DIRECTION('center_axis',(1.,0.,0.));
#34097=DIRECTION('ref_axis',(0.,0.,-1.));
#34098=DIRECTION('center_axis',(1.,0.,0.));
#34099=DIRECTION('ref_axis',(0.,0.,-1.));
#34100=DIRECTION('center_axis',(1.,0.,0.));
#34101=DIRECTION('ref_axis',(0.,1.,0.));
#34102=DIRECTION('',(-1.,0.,0.));
#34103=DIRECTION('center_axis',(1.,0.,0.));
#34104=DIRECTION('ref_axis',(0.,0.,-1.));
#34105=DIRECTION('center_axis',(-1.,0.,0.));
#34106=DIRECTION('ref_axis',(0.,0.,1.));
#34107=DIRECTION('center_axis',(1.,0.,0.));
#34108=DIRECTION('ref_axis',(0.,0.,-1.));
#34109=DIRECTION('center_axis',(1.,0.,0.));
#34110=DIRECTION('ref_axis',(0.,1.,0.));
#34111=DIRECTION('',(-1.,0.,0.));
#34112=DIRECTION('center_axis',(1.,0.,0.));
#34113=DIRECTION('ref_axis',(0.,0.,-1.));
#34114=DIRECTION('center_axis',(1.,0.,0.));
#34115=DIRECTION('ref_axis',(0.,0.,-1.));
#63479=CARTESIAN_POINT('',(0.,0.,0.));
#63480=CARTESIAN_POINT('Origin',(8.34,0.,26.5));
#63481=CARTESIAN_POINT('',(8.3,-1.49,26.5));
#63482=CARTESIAN_POINT('Origin',(8.3,0.,26.5));
#63483=CARTESIAN_POINT('',(8.37,-1.56,26.5));
#63484=CARTESIAN_POINT('',(8.34,-1.53,26.5));
#63485=CARTESIAN_POINT('Origin',(8.37,0.,26.5));
#63486=CARTESIAN_POINT('Origin',(8.26,0.,26.5));
#63487=CARTESIAN_POINT('',(8.23,-1.56,26.5));
#63488=CARTESIAN_POINT('Origin',(8.23,0.,26.5));
#63489=CARTESIAN_POINT('',(8.26,-1.53,26.5));
#63490=CARTESIAN_POINT('Origin',(8.3,0.,26.5));
#63491=CARTESIAN_POINT('',(8.15,-1.56,26.5));
#63492=CARTESIAN_POINT('',(8.3,-1.56,26.5));
#63493=CARTESIAN_POINT('Origin',(8.15,0.,26.5));
#63494=CARTESIAN_POINT('Origin',(7.975,0.,26.5));
#63495=CARTESIAN_POINT('',(8.15,-1.05,26.5));
#63496=CARTESIAN_POINT('Origin',(8.15,0.,26.5));
#63497=CARTESIAN_POINT('',(7.8,-1.05,26.5));
#63498=CARTESIAN_POINT('',(7.975,-1.05,26.5));
#63499=CARTESIAN_POINT('Origin',(7.8,0.,26.5));
#63500=CARTESIAN_POINT('Origin',(7.8,1.7,26.5));
#63501=CARTESIAN_POINT('',(7.8,-1.7,26.5));
#63502=CARTESIAN_POINT('Origin',(7.8,0.,26.5));
#63503=CARTESIAN_POINT('Origin',(7.825,0.,26.5));
#63504=CARTESIAN_POINT('',(7.85,-1.75,26.5));
#63505=CARTESIAN_POINT('Origin',(7.85,0.,26.5));
#63506=CARTESIAN_POINT('',(7.825,-1.725,26.5));
#63507=CARTESIAN_POINT('Origin',(8.,0.,26.5));
#63508=CARTESIAN_POINT('',(8.15,-1.75,26.5));
#63509=CARTESIAN_POINT('Origin',(8.15,0.,26.5));
#63510=CARTESIAN_POINT('',(8.,-1.75,26.5));
#63511=CARTESIAN_POINT('Origin',(8.15,1.56,26.5));
#63512=CARTESIAN_POINT('Origin',(8.3,0.,26.5));
#63513=CARTESIAN_POINT('',(8.45,-1.56,26.5));
#63514=CARTESIAN_POINT('Origin',(8.45,0.,26.5));
#63515=CARTESIAN_POINT('',(8.3,-1.56,26.5));
#63516=CARTESIAN_POINT('Origin',(8.45,1.72,26.5));
#63517=CARTESIAN_POINT('',(8.45,-1.72,26.5));
#63518=CARTESIAN_POINT('Origin',(8.45,0.,26.5));
#63519=CARTESIAN_POINT('Origin',(8.6,0.,26.5));
#63520=CARTESIAN_POINT('',(8.75,-1.72,26.5));
#63521=CARTESIAN_POINT('Origin',(8.75,0.,26.5));
#63522=CARTESIAN_POINT('',(8.6,-1.72,26.5));
#63523=CARTESIAN_POINT('Origin',(8.775,0.,26.5));
#63524=CARTESIAN_POINT('',(8.8,-1.67,26.5));
#63525=CARTESIAN_POINT('Origin',(8.8,0.,26.5));
#63526=CARTESIAN_POINT('',(8.775,-1.695,26.5));
#63527=CARTESIAN_POINT('Origin',(8.8,1.,26.5));
#63528=CARTESIAN_POINT('',(8.8,-1.,26.5));
#63529=CARTESIAN_POINT('Origin',(8.8,0.,26.5));
#63530=CARTESIAN_POINT('Origin',(8.625,0.,26.5));
#63531=CARTESIAN_POINT('',(8.45,-1.,26.5));
#63532=CARTESIAN_POINT('',(8.625,-1.,26.5));
#63533=CARTESIAN_POINT('Origin',(8.45,0.,26.5));
#63534=CARTESIAN_POINT('Origin',(8.45,1.24,26.5));
#63535=CARTESIAN_POINT('',(8.45,-1.24,26.5));
#63536=CARTESIAN_POINT('Origin',(8.45,0.,26.5));
#63537=CARTESIAN_POINT('Origin',(8.3,0.,26.5));
#63538=CARTESIAN_POINT('',(8.15,-1.24,26.5));
#63539=CARTESIAN_POINT('',(8.3,-1.24,26.5));
#63540=CARTESIAN_POINT('Origin',(8.15,0.,26.5));
#63541=CARTESIAN_POINT('Origin',(8.15,1.05,26.5));
#76634=UNCERTAINTY_MEASURE_WITH_UNIT(LENGTH_MEASURE(0.001),#76661,
'DISTANCE_ACCURACY_VALUE',
'Maximum model space distance between geometric entities at asserted c
onnectivities');
#76638=UNCERTAINTY_MEASURE_WITH_UNIT(LENGTH_MEASURE(0.001),#76661,
'DISTANCE_ACCURACY_VALUE',
'Maximum model space distance between geometric entities at asserted c
onnectivities');
#76656=(
GEOMETRIC_REPRESENTATION_CONTEXT(3)
GLOBAL_UNCERTAINTY_ASSIGNED_CONTEXT((#76634))
GLOBAL_UNIT_ASSIGNED_CONTEXT((#76661,#76663,#76664))
REPRESENTATION_CONTEXT('','3D')
);
#76660=(
GEOMETRIC_REPRESENTATION_CONTEXT(3)
GLOBAL_UNCERTAINTY_ASSIGNED_CONTEXT((#76638))
GLOBAL_UNIT_ASSIGNED_CONTEXT((#76661,#76663,#76664))
REPRESENTATION_CONTEXT('','3D')
);
#76661=(
LENGTH_UNIT()
NAMED_UNIT(*)
SI_UNIT(.CENTI.,.METRE.)
);
#76663=(
NAMED_UNIT(*)
PLANE_ANGLE_UNIT()
SI_UNIT($,.RADIAN.)
);
#76664=(
NAMED_UNIT(*)
SI_UNIT($,.STERADIAN.)
SOLID_ANGLE_UNIT()
);
#76682=SHAPE_DEFINITION_REPRESENTATION(#76703,#76752);
#76703=PRODUCT_DEFINITION_SHAPE('',$,#76774);
#76752=SHAPE_REPRESENTATION('',(#28525),#76656);
#76756=PRODUCT_DEFINITION_CONTEXT('part definition',#76821,'design');
#76774=PRODUCT_DEFINITION('2026-10-26-11-12-53-512',
'08_Thrust_Ball_Bearing_51104_20x35x10',#76795,#76756);
#76795=PRODUCT_DEFINITION_FORMATION('',$,#76840);
#76821=APPLICATION_CONTEXT(
'Core Data for Automotive Mechanical Design Process');
#76822=PRODUCT_CONTEXT('part definition',#76821,'mechanical');
#76840=PRODUCT('2026-10-26-11-12-53-512',
'08_Thrust_Ball_Bearing_51104_20x35x10',$,(#76822));
#76900=COLOUR_RGB('Grey',0.48,0.52,0.57);
#76901=FILL_AREA_STYLE_COLOUR('',#76900);
#76902=FILL_AREA_STYLE('',(#76901));
#76903=SURFACE_STYLE_FILL_AREA(#76902);
#76904=SURFACE_SIDE_STYLE('',(#76903));
#76905=SURFACE_STYLE_USAGE(.BOTH.,#76904);
#76906=PRESENTATION_STYLE_ASSIGNMENT((#76905));
ENDSEC;
END-ISO-10303-21;
